ISO-10303-21;
HEADER;
/* Generated by software containing ST-Developer
 * from STEP Tools, Inc. (www.steptools.com) 
 */

FILE_DESCRIPTION(
/* description */ ('Cam-and-follower valve demonstrator'),
/* implementation_level */ '2;1');

FILE_NAME(
/* name */ 'Inner race sleeve 10 mm (1).step',
/* time_stamp */ '2026-10-28T03:25:17-07:00',
/* author */ (''),
/* organization */ (''),
/* preprocessor_version */ 'ST-DEVELOPER v20.2',
/* originating_system */ 'Autodesk Translation Framework v15.17.0.0',
/* authorisation */ '');

FILE_SCHEMA (('AUTOMOTIVE_DESIGN { 1 0 10303 214 3 1 1 }'));
ENDSEC;

DATA;
#10=MECHANICAL_DESIGN_GEOMETRIC_PRESENTATION_REPRESENTATION('',(#442),#12896);
#363=SHAPE_REPRESENTATION_RELATIONSHIP('SRR','None',#13082,#399);
#399=ADVANCED_BREP_SHAPE_REPRESENTATION('',(#483),#12882);
#442=STYLED_ITEM('',(#13330),#483);
#483=MANIFOLD_SOLID_BREP('Body1',#6211);
#632=FACE_BOUND('',#1877,.T.);
#633=FACE_BOUND('',#1879,.T.);
#911=CIRCLE('',#7184,0.605);
#912=CIRCLE('',#7185,0.605);
#913=CIRCLE('',#7187,0.8);
#914=CIRCLE('',#7188,0.8);
#1067=CYLINDRICAL_SURFACE('',#7183,0.605);
#1068=CYLINDRICAL_SURFACE('',#7186,0.8);
#1369=FACE_OUTER_BOUND('',#1874,.T.);
#1370=FACE_OUTER_BOUND('',#1875,.T.);
#1371=FACE_OUTER_BOUND('',#1876,.T.);
#1372=FACE_OUTER_BOUND('',#1878,.T.);
#1874=EDGE_LOOP('',(#5251,#5252,#5253,#5254));
#1875=EDGE_LOOP('',(#5255,#5256,#5257,#5258));
#1876=EDGE_LOOP('',(#5259));
#1877=EDGE_LOOP('',(#5260));
#1878=EDGE_LOOP('',(#5261));
#1879=EDGE_LOOP('',(#5262));
#2306=LINE('',#12359,#2728);
#2307=LINE('',#12365,#2729);
#2728=VECTOR('',#8851,0.605);
#2729=VECTOR('',#8858,0.8);
#3230=VERTEX_POINT('',#12356);
#3231=VERTEX_POINT('',#12358);
#3232=VERTEX_POINT('',#12362);
#3233=VERTEX_POINT('',#12364);
#3922=EDGE_CURVE('',#3230,#3230,#911,.T.);
#3923=EDGE_CURVE('',#3230,#3231,#2306,.T.);
#3924=EDGE_CURVE('',#3231,#3231,#912,.T.);
#3925=EDGE_CURVE('',#3232,#3232,#913,.T.);
#3926=EDGE_CURVE('',#3232,#3233,#2307,.T.);
#3927=EDGE_CURVE('',#3233,#3233,#914,.T.);
#5251=ORIENTED_EDGE('',*,*,#3922,.F.);
#5252=ORIENTED_EDGE('',*,*,#3923,.T.);
#5253=ORIENTED_EDGE('',*,*,#3924,.T.);
#5254=ORIENTED_EDGE('',*,*,#3923,.F.);
#5255=ORIENTED_EDGE('',*,*,#3925,.F.);
#5256=ORIENTED_EDGE('',*,*,#3926,.T.);
#5257=ORIENTED_EDGE('',*,*,#3927,.T.);
#5258=ORIENTED_EDGE('',*,*,#3926,.F.);
#5259=ORIENTED_EDGE('',*,*,#3925,.T.);
#5260=ORIENTED_EDGE('',*,*,#3922,.T.);
#5261=ORIENTED_EDGE('',*,*,#3927,.F.);
#5262=ORIENTED_EDGE('',*,*,#3924,.F.);
#5749=PLANE('',#7189);
#5750=PLANE('',#7190);
#6085=ADVANCED_FACE('',(#1369),#1067,.F.);
#6086=ADVANCED_FACE('',(#1370),#1068,.T.);
#6087=ADVANCED_FACE('',(#1371,#632),#5749,.T.);
#6088=ADVANCED_FACE('',(#1372,#633),#5750,.F.);
#6211=CLOSED_SHELL('',(#6085,#6086,#6087,#6088));
#7182=AXIS2_PLACEMENT_3D('',#12354,#8845,#8846);
#7183=AXIS2_PLACEMENT_3D('',#12355,#8847,#8848);
#7184=AXIS2_PLACEMENT_3D('',#12357,#8849,#8850);
#7185=AXIS2_PLACEMENT_3D('',#12360,#8852,#8853);
#7186=AXIS2_PLACEMENT_3D('',#12361,#8854,#8855);
#7187=AXIS2_PLACEMENT_3D('',#12363,#8856,#8857);
#7188=AXIS2_PLACEMENT_3D('',#12366,#8859,#8860);
#7189=AXIS2_PLACEMENT_3D('',#12367,#8861,#8862);
#7190=AXIS2_PLACEMENT_3D('',#12368,#8863,#8864);
#8845=DIRECTION('axis',(0.,0.,1.));
#8846=DIRECTION('refdir',(1.,0.,0.));
#8847=DIRECTION('center_axis',(0.,1.,0.));
#8848=DIRECTION('ref_axis',(1.,0.,0.));
#8849=DIRECTION('center_axis',(0.,-1.,0.));
#8850=DIRECTION('ref_axis',(1.,0.,0.));
#8851=DIRECTION('',(0.,-1.,0.));
#8852=DIRECTION('center_axis',(0.,-1.,0.));
#8853=DIRECTION('ref_axis',(1.,0.,0.));
#8854=DIRECTION('center_axis',(0.,1.,0.));
#8855=DIRECTION('ref_axis',(1.,0.,0.));
#8856=DIRECTION('center_axis',(0.,1.,0.));
#8857=DIRECTION('ref_axis',(1.,0.,0.));
#8858=DIRECTION('',(0.,-1.,0.));
#8859=DIRECTION('center_axis',(0.,1.,0.));
#8860=DIRECTION('ref_axis',(1.,0.,0.));
#8861=DIRECTION('center_axis',(0.,1.,0.));
#8862=DIRECTION('ref_axis',(1.,0.,0.));
#8863=DIRECTION('center_axis',(0.,1.,0.));
#8864=DIRECTION('ref_axis',(1.,0.,0.));
#12354=CARTESIAN_POINT('',(0.,0.,0.));
#12355=CARTESIAN_POINT('Origin',(0.,1.,4.));
#12356=CARTESIAN_POINT('',(-0.605,2.,4.));
#12357=CARTESIAN_POINT('Origin',(0.,2.,4.));
#12358=CARTESIAN_POINT('',(-0.605,1.,4.));
#12359=CARTESIAN_POINT('',(-0.605,1.,4.));
#12360=CARTESIAN_POINT('Origin',(0.,1.,4.));
#12361=CARTESIAN_POINT('Origin',(0.,1.,4.));
#12362=CARTESIAN_POINT('',(-0.8,2.,4.));
#12363=CARTESIAN_POINT('Origin',(0.,2.,4.));
#12364=CARTESIAN_POINT('',(-0.8,1.,4.));
#12365=CARTESIAN_POINT('',(-0.8,1.,4.));
#12366=CARTESIAN_POINT('Origin',(0.,1.,4.));
#12367=CARTESIAN_POINT('Origin',(0.,2.,4.));
#12368=CARTESIAN_POINT('Origin',(0.,1.,4.));
#12839=UNCERTAINTY_MEASURE_WITH_UNIT(LENGTH_MEASURE(0.001),#12897,
'DISTANCE_ACCURACY_VALUE',
'Maximum model space distance between geometric entities at asserted c
onnectivities');
#12853=UNCERTAINTY_MEASURE_WITH_UNIT(LENGTH_MEASURE(0.001),#12897,
'DISTANCE_ACCURACY_VALUE',
'Maximum model space distance between geometric entities at asserted c
onnectivities');
#12882=(
GEOMETRIC_REPRESENTATION_CONTEXT(3)
GLOBAL_UNCERTAINTY_ASSIGNED_CONTEXT((#12839))
GLOBAL_UNIT_ASSIGNED_CONTEXT((#12897,#12899,#12900))
REPRESENTATION_CONTEXT('','3D')
);
#12896=(
GEOMETRIC_REPRESENTATION_CONTEXT(3)
GLOBAL_UNCERTAINTY_ASSIGNED_CONTEXT((#12853))
GLOBAL_UNIT_ASSIGNED_CONTEXT((#12897,#12899,#12900))
REPRESENTATION_CONTEXT('','3D')
);
#12897=(
LENGTH_UNIT()
NAMED_UNIT(*)
SI_UNIT(.CENTI.,.METRE.)
);
#12899=(
NAMED_UNIT(*)
PLANE_ANGLE_UNIT()
SI_UNIT($,.RADIAN.)
);
#12900=(
NAMED_UNIT(*)
SI_UNIT($,.STERADIAN.)
SOLID_ANGLE_UNIT()
);
#12929=SHAPE_DEFINITION_REPRESENTATION(#12978,#13082);
#12978=PRODUCT_DEFINITION_SHAPE('',$,#13125);
#13082=SHAPE_REPRESENTATION('',(#7182),#12882);
#13096=PRODUCT_DEFINITION_CONTEXT('part definition',#13224,'design');
#13125=PRODUCT_DEFINITION('Inner race sleeve 10 mm (1)',
'Inner race sleeve 10 mm (1)',#13167,#13096);
#13167=PRODUCT_DEFINITION_FORMATION('',$,#13254);
#13224=APPLICATION_CONTEXT(
'Core Data for Automotive Mechanical Design Process');
#13225=PRODUCT_CONTEXT('part definition',#13224,'mechanical');
#13254=PRODUCT('Inner race sleeve 10 mm (1)',
'Inner race sleeve 10 mm (1)','Inner race sleeve 10 mm (1)',(#13225));
#13324=COLOUR_RGB('Grey',0.48,0.52,0.57);
#13325=FILL_AREA_STYLE_COLOUR('',#13324);
#13326=FILL_AREA_STYLE('',(#13325));
#13327=SURFACE_STYLE_FILL_AREA(#13326);
#13328=SURFACE_SIDE_STYLE('',(#13327));
#13329=SURFACE_STYLE_USAGE(.BOTH.,#13328);
#13330=PRESENTATION_STYLE_ASSIGNMENT((#13329));
ENDSEC;
END-ISO-10303-21;
